ISO-10303-21;
HEADER;
/* Generated by software containing ST-Developer
 * from STEP Tools, Inc. (www.steptools.com) 
 */

FILE_DESCRIPTION(
/* description */ ('STEP AP214'),
/* implementation_level */ '2;1');

FILE_NAME(
/* name */ 'BO26-002_O Ring_End Cap O-ring.step',
/* time_stamp */ '2026-10-07T12:49:37-07:00',
/* author */ (''),
/* organization */ (''),
/* preprocessor_version */ 'ST-DEVELOPER v20.2',
/* originating_system */ 'Autodesk Translation Framework v15.15.0.0',
/* authorisation */ '');

FILE_SCHEMA (('AUTOMOTIVE_DESIGN { 1 0 10303 214 3 1 1 }'));
ENDSEC;

DATA;
#10=MECHANICAL_DESIGN_GEOMETRIC_PRESENTATION_REPRESENTATION('',(#316),#33016);
#258=SHAPE_REPRESENTATION_RELATIONSHIP('SRR','None',#33153,#285);
#285=ADVANCED_BREP_SHAPE_REPRESENTATION('',(#343),#33014);
#316=STYLED_ITEM('',(#33287),#343);
#343=MANIFOLD_SOLID_BREP('Body1',#9967);
#405=TOROIDAL_SURFACE('',#11184,13.045,1.31);
#1554=FACE_OUTER_BOUND('',#2188,.T.);
#2188=EDGE_LOOP('',(#9104,#9105,#9106,#9107));
#2584=CIRCLE('',#11185,1.31);
#2585=CIRCLE('',#11186,11.735);
#4986=VERTEX_POINT('',#32775);
#6365=EDGE_CURVE('',#4986,#4986,#2584,.T.);
#6366=EDGE_CURVE('',#4986,#4986,#2585,.T.);
#9104=ORIENTED_EDGE('',*,*,#6365,.F.);
#9105=ORIENTED_EDGE('',*,*,#6366,.T.);
#9106=ORIENTED_EDGE('',*,*,#6365,.T.);
#9107=ORIENTED_EDGE('',*,*,#6366,.F.);
#9920=ADVANCED_FACE('',(#1554),#405,.T.);
#9967=CLOSED_SHELL('',(#9920));
#11183=AXIS2_PLACEMENT_3D('',#32773,#13796,#13797);
#11184=AXIS2_PLACEMENT_3D('',#32774,#13798,#13799);
#11185=AXIS2_PLACEMENT_3D('',#32776,#13800,#13801);
#11186=AXIS2_PLACEMENT_3D('',#32777,#13802,#13803);
#13796=DIRECTION('axis',(0.,0.,1.));
#13797=DIRECTION('refdir',(1.,0.,0.));
#13798=DIRECTION('center_axis',(0.,1.,0.));
#13799=DIRECTION('ref_axis',(0.,0.,1.));
#13800=DIRECTION('center_axis',(-1.,0.,1.22464679914735E-16));
#13801=DIRECTION('ref_axis',(-1.22464679914735E-16,0.,-1.));
#13802=DIRECTION('center_axis',(0.,-1.,0.));
#13803=DIRECTION('ref_axis',(0.,0.,1.));
#32773=CARTESIAN_POINT('',(0.,0.,0.));
#32774=CARTESIAN_POINT('Origin',(0.,1.92592994438724E-31,0.));
#32775=CARTESIAN_POINT('',(-1.43712301879942E-15,1.60428730688303E-16,-11.735));
#32776=CARTESIAN_POINT('Origin',(-1.59755174948772E-15,1.92592994438724E-31,
-13.045));
#32777=CARTESIAN_POINT('Origin',(0.,-1.60428730688303E-16,0.));
#32982=UNCERTAINTY_MEASURE_WITH_UNIT(LENGTH_MEASURE(0.01),#33017,
'DISTANCE_ACCURACY_VALUE',
'Maximum model space distance between geometric entities at asserted c
onnectivities');
#32984=UNCERTAINTY_MEASURE_WITH_UNIT(LENGTH_MEASURE(0.01),#33017,
'DISTANCE_ACCURACY_VALUE',
'Maximum model space distance between geometric entities at asserted c
onnectivities');
#33014=(
GEOMETRIC_REPRESENTATION_CONTEXT(3)
GLOBAL_UNCERTAINTY_ASSIGNED_CONTEXT((#32982))
GLOBAL_UNIT_ASSIGNED_CONTEXT((#33017,#33019,#33020))
REPRESENTATION_CONTEXT('','3D')
);
#33016=(
GEOMETRIC_REPRESENTATION_CONTEXT(3)
GLOBAL_UNCERTAINTY_ASSIGNED_CONTEXT((#32984))
GLOBAL_UNIT_ASSIGNED_CONTEXT((#33017,#33019,#33020))
REPRESENTATION_CONTEXT('','3D')
);
#33017=(
LENGTH_UNIT()
NAMED_UNIT(*)
SI_UNIT(.MILLI.,.METRE.)
);
#33019=(
NAMED_UNIT(*)
PLANE_ANGLE_UNIT()
SI_UNIT($,.RADIAN.)
);
#33020=(
NAMED_UNIT(*)
SI_UNIT($,.STERADIAN.)
SOLID_ANGLE_UNIT()
);
#33050=SHAPE_DEFINITION_REPRESENTATION(#33112,#33153);
#33112=PRODUCT_DEFINITION_SHAPE('',$,#33185);
#33153=SHAPE_REPRESENTATION('',(#11183),#33014);
#33155=PRODUCT_DEFINITION_CONTEXT('part definition',#33250,'design');
#33185=PRODUCT_DEFINITION('BO26-002_O Ring_End Cap O-ring',
'BO26-002_O Ring_End Cap O-ring',#33216,#33155);
#33216=PRODUCT_DEFINITION_FORMATION('',$,#33281);
#33250=APPLICATION_CONTEXT(
'Core Data for Automotive Mechanical Design Process');
#33251=PRODUCT_CONTEXT('part definition',#33250,'mechanical');
#33281=PRODUCT('BO26-002_O Ring_End Cap O-ring',
'BO26-002_O Ring_End Cap O-ring',$,(#33251));
#33287=PRESENTATION_STYLE_ASSIGNMENT((#33294));
#33294=SURFACE_STYLE_USAGE(.BOTH.,#33301);
#33301=SURFACE_SIDE_STYLE('',(#33308));
#33308=SURFACE_STYLE_FILL_AREA(#33315);
#33315=FILL_AREA_STYLE('Opaque(76,76,76)',(#33322));
#33322=FILL_AREA_STYLE_COLOUR('Opaque(76,76,76)',#33329);
#33329=COLOUR_RGB('Opaque(76,76,76)', 0.31764706, 0.68627451, 0.89019608);
ENDSEC;
END-ISO-10303-21;
